ISO-10303-21;
HEADER;
/* Generated by software containing ST-Developer
 * from STEP Tools, Inc. (www.steptools.com) 
 */

FILE_DESCRIPTION(
/* description */ ('Torsion-spring ratchet demonstrator'),
/* implementation_level */ '2;1');

FILE_NAME(
/* name */ 'Socket Set Screw - M5x8.step',
/* time_stamp */ '2026-10-29T17:29:17-07:00',
/* author */ (''),
/* organization */ (''),
/* preprocessor_version */ 'ST-DEVELOPER v20.2',
/* originating_system */ 'Autodesk Translation Framework v15.17.0.0',
/* authorisation */ '');

FILE_SCHEMA (('AUTOMOTIVE_DESIGN { 1 0 10303 214 3 1 1 }'));
ENDSEC;

DATA;
#10=MECHANICAL_DESIGN_GEOMETRIC_PRESENTATION_REPRESENTATION('',(#313),#11258);
#197=CONICAL_SURFACE('',#6021,0.235,0.785398163397448);
#198=CONICAL_SURFACE('',#6025,0.2125,0.785398163397448);
#257=SHAPE_REPRESENTATION_RELATIONSHIP('SRR','None',#11385,#281);
#281=ADVANCED_BREP_SHAPE_REPRESENTATION('',(#343),#11255);
#313=STYLED_ITEM('',(#11591),#343);
#343=MANIFOLD_SOLID_BREP('Body1',#5186);
#434=FACE_BOUND('',#1302,.T.);
#602=PLANE('',#6012);
#603=PLANE('',#6013);
#604=PLANE('',#6014);
#605=PLANE('',#6015);
#606=PLANE('',#6016);
#607=PLANE('',#6017);
#608=PLANE('',#6018);
#609=PLANE('',#6019);
#610=PLANE('',#6027);
#900=FACE_OUTER_BOUND('',#1294,.T.);
#901=FACE_OUTER_BOUND('',#1295,.T.);
#902=FACE_OUTER_BOUND('',#1296,.T.);
#903=FACE_OUTER_BOUND('',#1297,.T.);
#904=FACE_OUTER_BOUND('',#1298,.T.);
#905=FACE_OUTER_BOUND('',#1299,.T.);
#906=FACE_OUTER_BOUND('',#1300,.T.);
#907=FACE_OUTER_BOUND('',#1301,.T.);
#908=FACE_OUTER_BOUND('',#1303,.T.);
#909=FACE_OUTER_BOUND('',#1304,.T.);
#910=FACE_OUTER_BOUND('',#1305,.T.);
#911=FACE_OUTER_BOUND('',#1306,.T.);
#1294=EDGE_LOOP('',(#4640,#4641,#4642,#4643));
#1295=EDGE_LOOP('',(#4644,#4645,#4646,#4647));
#1296=EDGE_LOOP('',(#4648,#4649,#4650,#4651));
#1297=EDGE_LOOP('',(#4652,#4653,#4654,#4655));
#1298=EDGE_LOOP('',(#4656,#4657,#4658,#4659));
#1299=EDGE_LOOP('',(#4660,#4661,#4662,#4663));
#1300=EDGE_LOOP('',(#4664,#4665,#4666,#4667,#4668,#4669));
#1301=EDGE_LOOP('',(#4670));
#1302=EDGE_LOOP('',(#4671,#4672,#4673,#4674,#4675,#4676));
#1303=EDGE_LOOP('',(#4677,#4678,#4679,#4680));
#1304=EDGE_LOOP('',(#4681,#4682,#4683,#4684));
#1305=EDGE_LOOP('',(#4685,#4686,#4687,#4688));
#1306=EDGE_LOOP('',(#4689));
#1660=LINE('',#11061,#2043);
#1661=LINE('',#11063,#2044);
#1662=LINE('',#11065,#2045);
#1663=LINE('',#11066,#2046);
#1664=LINE('',#11069,#2047);
#1665=LINE('',#11071,#2048);
#1666=LINE('',#11072,#2049);
#1667=LINE('',#11075,#2050);
#1668=LINE('',#11077,#2051);
#1669=LINE('',#11078,#2052);
#1670=LINE('',#11081,#2053);
#1671=LINE('',#11083,#2054);
#1672=LINE('',#11084,#2055);
#1673=LINE('',#11087,#2056);
#1674=LINE('',#11089,#2057);
#1675=LINE('',#11090,#2058);
#1676=LINE('',#11092,#2059);
#1677=LINE('',#11093,#2060);
#1678=LINE('',#11101,#2061);
#1679=LINE('',#11105,#2062);
#1680=LINE('',#11109,#2063);
#2043=VECTOR('',#7521,1.);
#2044=VECTOR('',#7522,1.);
#2045=VECTOR('',#7523,1.);
#2046=VECTOR('',#7524,1.);
#2047=VECTOR('',#7527,1.);
#2048=VECTOR('',#7528,1.);
#2049=VECTOR('',#7529,1.);
#2050=VECTOR('',#7532,1.);
#2051=VECTOR('',#7533,1.);
#2052=VECTOR('',#7534,1.);
#2053=VECTOR('',#7537,1.);
#2054=VECTOR('',#7538,1.);
#2055=VECTOR('',#7539,1.);
#2056=VECTOR('',#7542,1.);
#2057=VECTOR('',#7543,1.);
#2058=VECTOR('',#7544,1.);
#2059=VECTOR('',#7547,1.);
#2060=VECTOR('',#7548,1.);
#2061=VECTOR('',#7559,0.235);
#2062=VECTOR('',#7564,0.25);
#2063=VECTOR('',#7569,0.2125);
#2321=CIRCLE('',#6020,0.22);
#2322=CIRCLE('',#6022,0.24505);
#2323=CIRCLE('',#6024,0.24505);
#2324=CIRCLE('',#6026,0.175);
#2742=VERTEX_POINT('',#11059);
#2743=VERTEX_POINT('',#11060);
#2744=VERTEX_POINT('',#11062);
#2745=VERTEX_POINT('',#11064);
#2746=VERTEX_POINT('',#11068);
#2747=VERTEX_POINT('',#11070);
#2748=VERTEX_POINT('',#11074);
#2749=VERTEX_POINT('',#11076);
#2750=VERTEX_POINT('',#11080);
#2751=VERTEX_POINT('',#11082);
#2752=VERTEX_POINT('',#11086);
#2753=VERTEX_POINT('',#11088);
#2754=VERTEX_POINT('',#11096);
#2755=VERTEX_POINT('',#11099);
#2756=VERTEX_POINT('',#11103);
#2757=VERTEX_POINT('',#11107);
#3380=EDGE_CURVE('',#2742,#2743,#1660,.T.);
#3381=EDGE_CURVE('',#2742,#2744,#1661,.T.);
#3382=EDGE_CURVE('',#2744,#2745,#1662,.T.);
#3383=EDGE_CURVE('',#2743,#2745,#1663,.T.);
#3384=EDGE_CURVE('',#2746,#2742,#1664,.T.);
#3385=EDGE_CURVE('',#2746,#2747,#1665,.T.);
#3386=EDGE_CURVE('',#2747,#2744,#1666,.T.);
#3387=EDGE_CURVE('',#2748,#2746,#1667,.T.);
#3388=EDGE_CURVE('',#2748,#2749,#1668,.T.);
#3389=EDGE_CURVE('',#2749,#2747,#1669,.T.);
#3390=EDGE_CURVE('',#2750,#2748,#1670,.T.);
#3391=EDGE_CURVE('',#2750,#2751,#1671,.T.);
#3392=EDGE_CURVE('',#2751,#2749,#1672,.T.);
#3393=EDGE_CURVE('',#2752,#2750,#1673,.T.);
#3394=EDGE_CURVE('',#2752,#2753,#1674,.T.);
#3395=EDGE_CURVE('',#2753,#2751,#1675,.T.);
#3396=EDGE_CURVE('',#2743,#2752,#1676,.T.);
#3397=EDGE_CURVE('',#2745,#2753,#1677,.T.);
#3398=EDGE_CURVE('',#2754,#2754,#2321,.T.);
#3399=EDGE_CURVE('',#2755,#2755,#2322,.T.);
#3400=EDGE_CURVE('',#2755,#2754,#1678,.T.);
#3401=EDGE_CURVE('',#2756,#2756,#2323,.F.);
#3402=EDGE_CURVE('',#2756,#2755,#1679,.T.);
#3403=EDGE_CURVE('',#2757,#2757,#2324,.T.);
#3404=EDGE_CURVE('',#2757,#2756,#1680,.T.);
#4640=ORIENTED_EDGE('',*,*,#3380,.F.);
#4641=ORIENTED_EDGE('',*,*,#3381,.T.);
#4642=ORIENTED_EDGE('',*,*,#3382,.T.);
#4643=ORIENTED_EDGE('',*,*,#3383,.F.);
#4644=ORIENTED_EDGE('',*,*,#3384,.F.);
#4645=ORIENTED_EDGE('',*,*,#3385,.T.);
#4646=ORIENTED_EDGE('',*,*,#3386,.T.);
#4647=ORIENTED_EDGE('',*,*,#3381,.F.);
#4648=ORIENTED_EDGE('',*,*,#3387,.F.);
#4649=ORIENTED_EDGE('',*,*,#3388,.T.);
#4650=ORIENTED_EDGE('',*,*,#3389,.T.);
#4651=ORIENTED_EDGE('',*,*,#3385,.F.);
#4652=ORIENTED_EDGE('',*,*,#3390,.F.);
#4653=ORIENTED_EDGE('',*,*,#3391,.T.);
#4654=ORIENTED_EDGE('',*,*,#3392,.T.);
#4655=ORIENTED_EDGE('',*,*,#3388,.F.);
#4656=ORIENTED_EDGE('',*,*,#3393,.F.);
#4657=ORIENTED_EDGE('',*,*,#3394,.T.);
#4658=ORIENTED_EDGE('',*,*,#3395,.T.);
#4659=ORIENTED_EDGE('',*,*,#3391,.F.);
#4660=ORIENTED_EDGE('',*,*,#3396,.F.);
#4661=ORIENTED_EDGE('',*,*,#3383,.T.);
#4662=ORIENTED_EDGE('',*,*,#3397,.T.);
#4663=ORIENTED_EDGE('',*,*,#3394,.F.);
#4664=ORIENTED_EDGE('',*,*,#3397,.F.);
#4665=ORIENTED_EDGE('',*,*,#3382,.F.);
#4666=ORIENTED_EDGE('',*,*,#3386,.F.);
#4667=ORIENTED_EDGE('',*,*,#3389,.F.);
#4668=ORIENTED_EDGE('',*,*,#3392,.F.);
#4669=ORIENTED_EDGE('',*,*,#3395,.F.);
#4670=ORIENTED_EDGE('',*,*,#3398,.F.);
#4671=ORIENTED_EDGE('',*,*,#3380,.T.);
#4672=ORIENTED_EDGE('',*,*,#3396,.T.);
#4673=ORIENTED_EDGE('',*,*,#3393,.T.);
#4674=ORIENTED_EDGE('',*,*,#3390,.T.);
#4675=ORIENTED_EDGE('',*,*,#3387,.T.);
#4676=ORIENTED_EDGE('',*,*,#3384,.T.);
#4677=ORIENTED_EDGE('',*,*,#3399,.F.);
#4678=ORIENTED_EDGE('',*,*,#3400,.T.);
#4679=ORIENTED_EDGE('',*,*,#3398,.T.);
#4680=ORIENTED_EDGE('',*,*,#3400,.F.);
#4681=ORIENTED_EDGE('',*,*,#3401,.F.);
#4682=ORIENTED_EDGE('',*,*,#3402,.T.);
#4683=ORIENTED_EDGE('',*,*,#3399,.T.);
#4684=ORIENTED_EDGE('',*,*,#3402,.F.);
#4685=ORIENTED_EDGE('',*,*,#3403,.F.);
#4686=ORIENTED_EDGE('',*,*,#3404,.T.);
#4687=ORIENTED_EDGE('',*,*,#3401,.T.);
#4688=ORIENTED_EDGE('',*,*,#3404,.F.);
#4689=ORIENTED_EDGE('',*,*,#3403,.T.);
#4844=CYLINDRICAL_SURFACE('',#6023,0.24505);
#5126=ADVANCED_FACE('',(#900),#602,.F.);
#5127=ADVANCED_FACE('',(#901),#603,.F.);
#5128=ADVANCED_FACE('',(#902),#604,.F.);
#5129=ADVANCED_FACE('',(#903),#605,.F.);
#5130=ADVANCED_FACE('',(#904),#606,.F.);
#5131=ADVANCED_FACE('',(#905),#607,.F.);
#5132=ADVANCED_FACE('',(#906),#608,.F.);
#5133=ADVANCED_FACE('',(#907,#434),#609,.T.);
#5134=ADVANCED_FACE('',(#908),#197,.T.);
#5135=ADVANCED_FACE('',(#909),#4844,.T.);
#5136=ADVANCED_FACE('',(#910),#198,.T.);
#5137=ADVANCED_FACE('',(#911),#610,.T.);
#5186=CLOSED_SHELL('',(#5126,#5127,#5128,#5129,#5130,#5131,#5132,#5133,
#5134,#5135,#5136,#5137));
#6011=AXIS2_PLACEMENT_3D('',#11057,#7517,#7518);
#6012=AXIS2_PLACEMENT_3D('',#11058,#7519,#7520);
#6013=AXIS2_PLACEMENT_3D('',#11067,#7525,#7526);
#6014=AXIS2_PLACEMENT_3D('',#11073,#7530,#7531);
#6015=AXIS2_PLACEMENT_3D('',#11079,#7535,#7536);
#6016=AXIS2_PLACEMENT_3D('',#11085,#7540,#7541);
#6017=AXIS2_PLACEMENT_3D('',#11091,#7545,#7546);
#6018=AXIS2_PLACEMENT_3D('',#11094,#7549,#7550);
#6019=AXIS2_PLACEMENT_3D('',#11095,#7551,#7552);
#6020=AXIS2_PLACEMENT_3D('',#11097,#7553,#7554);
#6021=AXIS2_PLACEMENT_3D('',#11098,#7555,#7556);
#6022=AXIS2_PLACEMENT_3D('',#11100,#7557,#7558);
#6023=AXIS2_PLACEMENT_3D('',#11102,#7560,#7561);
#6024=AXIS2_PLACEMENT_3D('',#11104,#7562,#7563);
#6025=AXIS2_PLACEMENT_3D('',#11106,#7565,#7566);
#6026=AXIS2_PLACEMENT_3D('',#11108,#7567,#7568);
#6027=AXIS2_PLACEMENT_3D('',#11110,#7570,#7571);
#7517=DIRECTION('axis',(0.,0.,1.));
#7518=DIRECTION('refdir',(1.,0.,0.));
#7519=DIRECTION('center_axis',(0.866025403784439,0.,-0.5));
#7520=DIRECTION('ref_axis',(0.5,0.,0.866025403784439));
#7521=DIRECTION('',(0.5,0.,0.866025403784439));
#7522=DIRECTION('',(0.,-1.,0.));
#7523=DIRECTION('',(0.5,0.,0.866025403784439));
#7524=DIRECTION('',(0.,-1.,0.));
#7525=DIRECTION('center_axis',(1.92296268638356E-16,0.,-1.));
#7526=DIRECTION('ref_axis',(1.,0.,1.92296268638356E-16));
#7527=DIRECTION('',(1.,0.,1.92296268638356E-16));
#7528=DIRECTION('',(0.,-1.,0.));
#7529=DIRECTION('',(1.,0.,1.92296268638356E-16));
#7530=DIRECTION('center_axis',(-0.866025403784439,0.,-0.5));
#7531=DIRECTION('ref_axis',(0.5,0.,-0.866025403784439));
#7532=DIRECTION('',(0.5,0.,-0.866025403784439));
#7533=DIRECTION('',(0.,-1.,0.));
#7534=DIRECTION('',(0.5,0.,-0.866025403784438));
#7535=DIRECTION('center_axis',(-0.866025403784439,0.,0.5));
#7536=DIRECTION('ref_axis',(-0.5,0.,-0.866025403784439));
#7537=DIRECTION('',(-0.5,0.,-0.866025403784439));
#7538=DIRECTION('',(0.,-1.,0.));
#7539=DIRECTION('',(-0.5,0.,-0.866025403784439));
#7540=DIRECTION('center_axis',(-1.92296268638356E-16,0.,1.));
#7541=DIRECTION('ref_axis',(-1.,0.,-1.92296268638356E-16));
#7542=DIRECTION('',(-1.,0.,-1.92296268638356E-16));
#7543=DIRECTION('',(0.,-1.,0.));
#7544=DIRECTION('',(-1.,0.,-1.92296268638356E-16));
#7545=DIRECTION('center_axis',(0.866025403784439,0.,0.5));
#7546=DIRECTION('ref_axis',(-0.5,0.,0.866025403784439));
#7547=DIRECTION('',(-0.5,0.,0.866025403784439));
#7548=DIRECTION('',(-0.5,0.,0.866025403784439));
#7549=DIRECTION('center_axis',(0.,-1.,0.));
#7550=DIRECTION('ref_axis',(0.,0.,-1.));
#7551=DIRECTION('center_axis',(0.,1.,0.));
#7552=DIRECTION('ref_axis',(0.,0.,1.));
#7553=DIRECTION('center_axis',(0.,-1.,0.));
#7554=DIRECTION('ref_axis',(1.,0.,0.));
#7555=DIRECTION('center_axis',(0.,-1.,0.));
#7556=DIRECTION('ref_axis',(1.,0.,0.));
#7557=DIRECTION('center_axis',(0.,-1.,0.));
#7558=DIRECTION('ref_axis',(1.,0.,0.));
#7559=DIRECTION('',(0.707106781186547,0.707106781186548,8.65956056235493E-17));
#7560=DIRECTION('center_axis',(0.,-1.,0.));
#7561=DIRECTION('ref_axis',(1.,0.,0.));
#7562=DIRECTION('center_axis',(0.,1.,0.));
#7563=DIRECTION('ref_axis',(1.,0.,0.));
#7564=DIRECTION('',(0.,1.,0.));
#7565=DIRECTION('center_axis',(0.,1.,0.));
#7566=DIRECTION('ref_axis',(1.,0.,0.));
#7567=DIRECTION('center_axis',(0.,-1.,0.));
#7568=DIRECTION('ref_axis',(1.,0.,0.));
#7569=DIRECTION('',(-0.707106781186547,0.707106781186548,-8.65956056235493E-17));
#7570=DIRECTION('center_axis',(0.,-1.,0.));
#7571=DIRECTION('ref_axis',(0.,0.,-1.));
#11057=CARTESIAN_POINT('',(0.,0.,0.));
#11058=CARTESIAN_POINT('Origin',(0.0721687836487032,0.,-0.125));
#11059=CARTESIAN_POINT('',(0.0721687836487032,0.,-0.125));
#11060=CARTESIAN_POINT('',(0.144337567297406,0.,0.));
#11061=CARTESIAN_POINT('',(0.117710979560879,0.,-0.0461186027918559));
#11062=CARTESIAN_POINT('',(0.0721687836487032,-0.25,-0.125));
#11063=CARTESIAN_POINT('',(0.0721687836487032,0.,-0.125));
#11064=CARTESIAN_POINT('',(0.144337567297406,-0.25,0.));
#11065=CARTESIAN_POINT('',(0.144337567297406,-0.25,0.));
#11066=CARTESIAN_POINT('',(0.144337567297406,0.,0.));
#11067=CARTESIAN_POINT('Origin',(-0.0721687836487032,0.,-0.125));
#11068=CARTESIAN_POINT('',(-0.0721687836487032,0.,-0.125));
#11069=CARTESIAN_POINT('',(0.0739156081756484,0.,-0.125));
#11070=CARTESIAN_POINT('',(-0.0721687836487032,-0.25,-0.125));
#11071=CARTESIAN_POINT('',(-0.0721687836487032,0.,-0.125));
#11072=CARTESIAN_POINT('',(0.0721687836487032,-0.25,-0.125));
#11073=CARTESIAN_POINT('Origin',(-0.144337567297406,0.,-4.16333634234434E-17));
#11074=CARTESIAN_POINT('',(-0.144337567297406,0.,-1.76762539787485E-17));
#11075=CARTESIAN_POINT('',(-0.0987953713852306,0.,-0.0788813972081442));
#11076=CARTESIAN_POINT('',(-0.144337567297406,-0.25,-2.77555756156289E-17));
#11077=CARTESIAN_POINT('',(-0.144337567297406,0.,-1.76762539787485E-17));
#11078=CARTESIAN_POINT('',(-0.0721687836487032,-0.25,-0.125));
#11079=CARTESIAN_POINT('Origin',(-0.0721687836487033,0.,0.125));
#11080=CARTESIAN_POINT('',(-0.0721687836487033,0.,0.125));
#11081=CARTESIAN_POINT('',(-0.0627109795608791,0.,0.141381397208144));
#11082=CARTESIAN_POINT('',(-0.0721687836487033,-0.25,0.125));
#11083=CARTESIAN_POINT('',(-0.0721687836487033,0.,0.125));
#11084=CARTESIAN_POINT('',(-0.144337567297406,-0.25,-1.76762539787485E-17));
#11085=CARTESIAN_POINT('Origin',(0.0721687836487032,0.,0.125));
#11086=CARTESIAN_POINT('',(0.0721687836487032,0.,0.125));
#11087=CARTESIAN_POINT('',(0.146084391824352,0.,0.125));
#11088=CARTESIAN_POINT('',(0.0721687836487032,-0.25,0.125));
#11089=CARTESIAN_POINT('',(0.0721687836487032,0.,0.125));
#11090=CARTESIAN_POINT('',(-0.0721687836487033,-0.25,0.125));
#11091=CARTESIAN_POINT('Origin',(0.144337567297406,0.,0.));
#11092=CARTESIAN_POINT('',(0.153795371385231,0.,-0.0163813972081441));
#11093=CARTESIAN_POINT('',(0.0721687836487032,-0.25,0.125));
#11094=CARTESIAN_POINT('Origin',(0.,-0.25,0.));
#11095=CARTESIAN_POINT('Origin',(0.22,0.,0.));
#11096=CARTESIAN_POINT('',(-0.22,-8.67361737988404E-18,-2.69422295812418E-17));
#11097=CARTESIAN_POINT('Origin',(0.,0.,0.));
#11098=CARTESIAN_POINT('Origin',(0.,-0.015,0.));
#11099=CARTESIAN_POINT('',(-0.24505,-0.02505,-3.00099698131059E-17));
#11100=CARTESIAN_POINT('Origin',(0.,-0.02505,0.));
#11101=CARTESIAN_POINT('',(-0.235,-0.015,-2.87791997799628E-17));
#11102=CARTESIAN_POINT('Origin',(0.,-0.3775,0.));
#11103=CARTESIAN_POINT('',(-0.24505,-0.72995,3.00099698131059E-17));
#11104=CARTESIAN_POINT('Origin',(0.,-0.72995,0.));
#11105=CARTESIAN_POINT('',(-0.24505,-0.3775,-3.00099698131059E-17));
#11106=CARTESIAN_POINT('Origin',(0.,-0.7625,0.));
#11107=CARTESIAN_POINT('',(-0.175,-0.8,-2.14313189850787E-17));
#11108=CARTESIAN_POINT('Origin',(0.,-0.8,0.));
#11109=CARTESIAN_POINT('',(-0.2125,-0.7625,-2.60237444818813E-17));
#11110=CARTESIAN_POINT('Origin',(0.,-0.8,0.));
#11225=UNCERTAINTY_MEASURE_WITH_UNIT(LENGTH_MEASURE(0.001),#11259,
'DISTANCE_ACCURACY_VALUE',
'Maximum model space distance between geometric entities at asserted c
onnectivities');
#11228=UNCERTAINTY_MEASURE_WITH_UNIT(LENGTH_MEASURE(0.001),#11259,
'DISTANCE_ACCURACY_VALUE',
'Maximum model space distance between geometric entities at asserted c
onnectivities');
#11255=(
GEOMETRIC_REPRESENTATION_CONTEXT(3)
GLOBAL_UNCERTAINTY_ASSIGNED_CONTEXT((#11225))
GLOBAL_UNIT_ASSIGNED_CONTEXT((#11259,#11261,#11262))
REPRESENTATION_CONTEXT('','3D')
);
#11258=(
GEOMETRIC_REPRESENTATION_CONTEXT(3)
GLOBAL_UNCERTAINTY_ASSIGNED_CONTEXT((#11228))
GLOBAL_UNIT_ASSIGNED_CONTEXT((#11259,#11261,#11262))
REPRESENTATION_CONTEXT('','3D')
);
#11259=(
LENGTH_UNIT()
NAMED_UNIT(*)
SI_UNIT(.CENTI.,.METRE.)
);
#11261=(
NAMED_UNIT(*)
PLANE_ANGLE_UNIT()
SI_UNIT($,.RADIAN.)
);
#11262=(
NAMED_UNIT(*)
SI_UNIT($,.STERADIAN.)
SOLID_ANGLE_UNIT()
);
#11289=SHAPE_DEFINITION_REPRESENTATION(#11346,#11385);
#11346=PRODUCT_DEFINITION_SHAPE('',$,#11415);
#11385=SHAPE_REPRESENTATION('',(#6011),#11255);
#11388=PRODUCT_DEFINITION_CONTEXT('part definition',#11477,'design');
#11415=PRODUCT_DEFINITION('Socket Set Screw - M5x8',
'Socket Set Screw - M5x8',#11444,#11388);
#11444=PRODUCT_DEFINITION_FORMATION('',$,#11505);
#11477=APPLICATION_CONTEXT(
'Core Data for Automotive Mechanical Design Process');
#11478=PRODUCT_CONTEXT('part definition',#11477,'mechanical');
#11505=PRODUCT('Socket Set Screw - M5x8','Socket Set Screw - M5x8',
'Socket Set Screw - M5x8',(#11478));
#11585=COLOUR_RGB('Black',0.12,0.14,0.17);
#11586=FILL_AREA_STYLE_COLOUR('',#11585);
#11587=FILL_AREA_STYLE('',(#11586));
#11588=SURFACE_STYLE_FILL_AREA(#11587);
#11589=SURFACE_SIDE_STYLE('',(#11588));
#11590=SURFACE_STYLE_USAGE(.BOTH.,#11589);
#11591=PRESENTATION_STYLE_ASSIGNMENT((#11590));
ENDSEC;
END-ISO-10303-21;
